ISO-10303-21;
HEADER;
/* Generated by software containing ST-Developer
 * from STEP Tools, Inc. (www.steptools.com) 
 */

FILE_DESCRIPTION(
/* description */ (''),
/* implementation_level */ '2;1');

FILE_NAME(
/* name */ '13_Circlip_DIN_472_-_52.step',
/* time_stamp */ '2026-10-26T04:15:57-07:00',
/* author */ (''),
/* organization */ (''),
/* preprocessor_version */ 'ST-DEVELOPER v20.2',
/* originating_system */ 'Autodesk Translation Framework v15.15.0.0',
/* authorisation */ '');

FILE_SCHEMA (('AUTOMOTIVE_DESIGN { 1 0 10303 214 3 1 1 }'));
ENDSEC;

DATA;
#10=MECHANICAL_DESIGN_GEOMETRIC_PRESENTATION_REPRESENTATION('',(#464),#55737);
#163=(
BOUNDED_CURVE()
B_SPLINE_CURVE(2,(#45353,#45354,#45355),.UNSPECIFIED.,.F.,.F.)
B_SPLINE_CURVE_WITH_KNOTS((3,3),(0.25768579992867,0.284744725788376),
 .UNSPECIFIED.)
CURVE()
GEOMETRIC_REPRESENTATION_ITEM()
RATIONAL_B_SPLINE_CURVE((1.00026246290895,1.0001450117334,1.))
REPRESENTATION_ITEM('')
);
#164=(
BOUNDED_CURVE()
B_SPLINE_CURVE(2,(#45362,#45363,#45364),.UNSPECIFIED.,.F.,.F.)
B_SPLINE_CURVE_WITH_KNOTS((3,3),(0.,0.0284560379907694),.UNSPECIFIED.)
CURVE()
GEOMETRIC_REPRESENTATION_ITEM()
RATIONAL_B_SPLINE_CURVE((1.,1.00001378568341,1.))
REPRESENTATION_ITEM('')
);
#165=(
BOUNDED_CURVE()
B_SPLINE_CURVE(2,(#45374,#45375,#45376),.UNSPECIFIED.,.F.,.F.)
B_SPLINE_CURVE_WITH_KNOTS((3,3),(0.,0.0270589258586405),.UNSPECIFIED.)
CURVE()
GEOMETRIC_REPRESENTATION_ITEM()
RATIONAL_B_SPLINE_CURVE((1.,1.00014501173361,1.00026246290934))
REPRESENTATION_ITEM('')
);
#166=(
BOUNDED_CURVE()
B_SPLINE_CURVE(2,(#45385,#45386,#45387),.UNSPECIFIED.,.F.,.F.)
B_SPLINE_CURVE_WITH_KNOTS((3,3),(0.,0.0284560379907693),.UNSPECIFIED.)
CURVE()
GEOMETRIC_REPRESENTATION_ITEM()
RATIONAL_B_SPLINE_CURVE((1.,1.00001378474395,1.))
REPRESENTATION_ITEM('')
);
#334=ELLIPSE('',#29227,38.8908729652601,27.5);
#335=ELLIPSE('',#29234,38.8908729652601,27.5);
#336=ELLIPSE('',#29237,38.8908729652601,27.5);
#337=ELLIPSE('',#29243,38.8908729652601,27.5);
#381=CONICAL_SURFACE('',#29230,22.1,0.785398163397444);
#382=CONICAL_SURFACE('',#29238,22.1,0.785398163397444);
#424=SHAPE_REPRESENTATION_RELATIONSHIP('SRR','None',#55833,#444);
#444=ADVANCED_BREP_SHAPE_REPRESENTATION('',(#484),#55729);
#464=STYLED_ITEM('',(#55991),#484);
#484=MANIFOLD_SOLID_BREP('Body1',#27233);
#1405=PLANE('',#29224);
#1406=PLANE('',#29225);
#1407=PLANE('',#29226);
#1408=PLANE('',#29228);
#1409=PLANE('',#29229);
#1410=PLANE('',#29233);
#1411=PLANE('',#29235);
#1412=PLANE('',#29236);
#1413=PLANE('',#29241);
#1414=PLANE('',#29242);
#1415=PLANE('',#29244);
#1416=PLANE('',#29246);
#1417=PLANE('',#29250);
#1418=PLANE('',#29251);
#3352=LINE('',#45350,#5723);
#3353=LINE('',#45352,#5724);
#3354=LINE('',#45359,#5725);
#3355=LINE('',#45361,#5726);
#3356=LINE('',#45369,#5727);
#3357=LINE('',#45370,#5728);
#3358=LINE('',#45378,#5729);
#3359=LINE('',#45379,#5730);
#3360=LINE('',#45383,#5731);
#3361=LINE('',#45388,#5732);
#3362=LINE('',#45396,#5733);
#3363=LINE('',#45397,#5734);
#3364=LINE('',#45399,#5735);
#3365=LINE('',#45400,#5736);
#3366=LINE('',#45405,#5737);
#3367=LINE('',#45406,#5738);
#3368=LINE('',#45411,#5739);
#3369=LINE('',#45412,#5740);
#3370=LINE('',#45417,#5741);
#3371=LINE('',#45418,#5742);
#3372=LINE('',#45422,#5743);
#3373=LINE('',#45426,#5744);
#5723=VECTOR('',#35096,10.);
#5724=VECTOR('',#35097,10.);
#5725=VECTOR('',#35100,10.);
#5726=VECTOR('',#35101,10.);
#5727=VECTOR('',#35106,10.);
#5728=VECTOR('',#35107,10.);
#5729=VECTOR('',#35110,10.);
#5730=VECTOR('',#35111,10.);
#5731=VECTOR('',#35114,10.);
#5732=VECTOR('',#35115,10.);
#5733=VECTOR('',#35126,10.);
#5734=VECTOR('',#35127,10.);
#5735=VECTOR('',#35130,10.);
#5736=VECTOR('',#35131,10.);
#5737=VECTOR('',#35136,10.);
#5738=VECTOR('',#35137,10.);
#5739=VECTOR('',#35146,10.);
#5740=VECTOR('',#35147,10.);
#5741=VECTOR('',#35152,10.);
#5742=VECTOR('',#35153,10.);
#5743=VECTOR('',#35160,10.);
#5744=VECTOR('',#35167,10.);
#6696=CYLINDRICAL_SURFACE('',#29247,22.);
#6697=CYLINDRICAL_SURFACE('',#29248,27.5);
#7868=FACE_OUTER_BOUND('',#9537,.T.);
#7869=FACE_OUTER_BOUND('',#9538,.T.);
#7870=FACE_OUTER_BOUND('',#9539,.T.);
#7871=FACE_OUTER_BOUND('',#9540,.T.);
#7872=FACE_OUTER_BOUND('',#9541,.T.);
#7873=FACE_OUTER_BOUND('',#9542,.T.);
#7874=FACE_OUTER_BOUND('',#9543,.T.);
#7875=FACE_OUTER_BOUND('',#9544,.T.);
#7876=FACE_OUTER_BOUND('',#9545,.T.);
#7877=FACE_OUTER_BOUND('',#9546,.T.);
#7878=FACE_OUTER_BOUND('',#9547,.T.);
#7879=FACE_OUTER_BOUND('',#9548,.T.);
#7880=FACE_OUTER_BOUND('',#9549,.T.);
#7881=FACE_OUTER_BOUND('',#9550,.T.);
#7882=FACE_OUTER_BOUND('',#9551,.T.);
#7883=FACE_OUTER_BOUND('',#9552,.T.);
#7884=FACE_OUTER_BOUND('',#9553,.T.);
#7885=FACE_OUTER_BOUND('',#9554,.T.);
#9537=EDGE_LOOP('',(#23058,#23059,#23060));
#9538=EDGE_LOOP('',(#23061,#23062,#23063));
#9539=EDGE_LOOP('',(#23064,#23065,#23066,#23067));
#9540=EDGE_LOOP('',(#23068,#23069,#23070));
#9541=EDGE_LOOP('',(#23071,#23072,#23073));
#9542=EDGE_LOOP('',(#23074,#23075,#23076,#23077));
#9543=EDGE_LOOP('',(#23078,#23079,#23080,#23081));
#9544=EDGE_LOOP('',(#23082,#23083,#23084,#23085));
#9545=EDGE_LOOP('',(#23086,#23087,#23088,#23089));
#9546=EDGE_LOOP('',(#23090,#23091,#23092,#23093));
#9547=EDGE_LOOP('',(#23094,#23095,#23096,#23097));
#9548=EDGE_LOOP('',(#23098,#23099,#23100,#23101));
#9549=EDGE_LOOP('',(#23102,#23103,#23104,#23105));
#9550=EDGE_LOOP('',(#23106,#23107,#23108,#23109));
#9551=EDGE_LOOP('',(#23110,#23111,#23112,#23113));
#9552=EDGE_LOOP('',(#23114,#23115,#23116,#23117,#23118,#23119,#23120,#23121));
#9553=EDGE_LOOP('',(#23122,#23123,#23124,#23125));
#9554=EDGE_LOOP('',(#23126,#23127,#23128,#23129));
#10788=CIRCLE('',#29231,22.2);
#10789=CIRCLE('',#29232,22.);
#10790=CIRCLE('',#29239,22.2);
#10791=CIRCLE('',#29240,22.);
#10792=CIRCLE('',#29245,27.5);
#10793=CIRCLE('',#29249,27.5);
#13108=VERTEX_POINT('',#45348);
#13109=VERTEX_POINT('',#45349);
#13110=VERTEX_POINT('',#45351);
#13111=VERTEX_POINT('',#45357);
#13112=VERTEX_POINT('',#45358);
#13113=VERTEX_POINT('',#45360);
#13114=VERTEX_POINT('',#45366);
#13115=VERTEX_POINT('',#45367);
#13116=VERTEX_POINT('',#45372);
#13117=VERTEX_POINT('',#45373);
#13118=VERTEX_POINT('',#45377);
#13119=VERTEX_POINT('',#45381);
#13120=VERTEX_POINT('',#45382);
#13121=VERTEX_POINT('',#45384);
#13122=VERTEX_POINT('',#45393);
#13123=VERTEX_POINT('',#45394);
#13124=VERTEX_POINT('',#45402);
#13125=VERTEX_POINT('',#45403);
#13126=VERTEX_POINT('',#45414);
#13127=VERTEX_POINT('',#45415);
#16533=EDGE_CURVE('',#13108,#13109,#3352,.T.);
#16534=EDGE_CURVE('',#13110,#13108,#3353,.T.);
#16535=EDGE_CURVE('',#13109,#13110,#163,.F.);
#16536=EDGE_CURVE('',#13111,#13112,#3354,.T.);
#16537=EDGE_CURVE('',#13113,#13111,#3355,.T.);
#16538=EDGE_CURVE('',#13112,#13113,#164,.F.);
#16539=EDGE_CURVE('',#13114,#13115,#334,.T.);
#16540=EDGE_CURVE('',#13115,#13113,#3356,.T.);
#16541=EDGE_CURVE('',#13111,#13114,#3357,.T.);
#16542=EDGE_CURVE('',#13116,#13117,#165,.F.);
#16543=EDGE_CURVE('',#13118,#13116,#3358,.T.);
#16544=EDGE_CURVE('',#13117,#13118,#3359,.T.);
#16545=EDGE_CURVE('',#13119,#13120,#3360,.T.);
#16546=EDGE_CURVE('',#13121,#13119,#166,.F.);
#16547=EDGE_CURVE('',#13120,#13121,#3361,.T.);
#16548=EDGE_CURVE('',#13113,#13121,#10788,.T.);
#16549=EDGE_CURVE('',#13119,#13112,#10789,.T.);
#16550=EDGE_CURVE('',#13122,#13123,#335,.T.);
#16551=EDGE_CURVE('',#13123,#13120,#3362,.T.);
#16552=EDGE_CURVE('',#13121,#13122,#3363,.T.);
#16553=EDGE_CURVE('',#13116,#13119,#3364,.T.);
#16554=EDGE_CURVE('',#13120,#13118,#3365,.T.);
#16555=EDGE_CURVE('',#13124,#13125,#336,.T.);
#16556=EDGE_CURVE('',#13125,#13117,#3366,.T.);
#16557=EDGE_CURVE('',#13118,#13124,#3367,.T.);
#16558=EDGE_CURVE('',#13117,#13109,#10790,.T.);
#16559=EDGE_CURVE('',#13110,#13116,#10791,.T.);
#16560=EDGE_CURVE('',#13108,#13111,#3368,.T.);
#16561=EDGE_CURVE('',#13112,#13110,#3369,.T.);
#16562=EDGE_CURVE('',#13126,#13127,#337,.T.);
#16563=EDGE_CURVE('',#13127,#13108,#3370,.T.);
#16564=EDGE_CURVE('',#13109,#13126,#3371,.T.);
#16565=EDGE_CURVE('',#13122,#13115,#10792,.T.);
#16566=EDGE_CURVE('',#13114,#13127,#3372,.T.);
#16567=EDGE_CURVE('',#13125,#13126,#10793,.T.);
#16568=EDGE_CURVE('',#13123,#13124,#3373,.T.);
#23058=ORIENTED_EDGE('',*,*,#16533,.F.);
#23059=ORIENTED_EDGE('',*,*,#16534,.F.);
#23060=ORIENTED_EDGE('',*,*,#16535,.F.);
#23061=ORIENTED_EDGE('',*,*,#16536,.F.);
#23062=ORIENTED_EDGE('',*,*,#16537,.F.);
#23063=ORIENTED_EDGE('',*,*,#16538,.F.);
#23064=ORIENTED_EDGE('',*,*,#16539,.T.);
#23065=ORIENTED_EDGE('',*,*,#16540,.T.);
#23066=ORIENTED_EDGE('',*,*,#16537,.T.);
#23067=ORIENTED_EDGE('',*,*,#16541,.T.);
#23068=ORIENTED_EDGE('',*,*,#16542,.F.);
#23069=ORIENTED_EDGE('',*,*,#16543,.F.);
#23070=ORIENTED_EDGE('',*,*,#16544,.F.);
#23071=ORIENTED_EDGE('',*,*,#16545,.F.);
#23072=ORIENTED_EDGE('',*,*,#16546,.F.);
#23073=ORIENTED_EDGE('',*,*,#16547,.F.);
#23074=ORIENTED_EDGE('',*,*,#16538,.T.);
#23075=ORIENTED_EDGE('',*,*,#16548,.T.);
#23076=ORIENTED_EDGE('',*,*,#16546,.T.);
#23077=ORIENTED_EDGE('',*,*,#16549,.T.);
#23078=ORIENTED_EDGE('',*,*,#16550,.T.);
#23079=ORIENTED_EDGE('',*,*,#16551,.T.);
#23080=ORIENTED_EDGE('',*,*,#16547,.T.);
#23081=ORIENTED_EDGE('',*,*,#16552,.T.);
#23082=ORIENTED_EDGE('',*,*,#16543,.T.);
#23083=ORIENTED_EDGE('',*,*,#16553,.T.);
#23084=ORIENTED_EDGE('',*,*,#16545,.T.);
#23085=ORIENTED_EDGE('',*,*,#16554,.T.);
#23086=ORIENTED_EDGE('',*,*,#16555,.T.);
#23087=ORIENTED_EDGE('',*,*,#16556,.T.);
#23088=ORIENTED_EDGE('',*,*,#16544,.T.);
#23089=ORIENTED_EDGE('',*,*,#16557,.T.);
#23090=ORIENTED_EDGE('',*,*,#16542,.T.);
#23091=ORIENTED_EDGE('',*,*,#16558,.T.);
#23092=ORIENTED_EDGE('',*,*,#16535,.T.);
#23093=ORIENTED_EDGE('',*,*,#16559,.T.);
#23094=ORIENTED_EDGE('',*,*,#16534,.T.);
#23095=ORIENTED_EDGE('',*,*,#16560,.T.);
#23096=ORIENTED_EDGE('',*,*,#16536,.T.);
#23097=ORIENTED_EDGE('',*,*,#16561,.T.);
#23098=ORIENTED_EDGE('',*,*,#16562,.T.);
#23099=ORIENTED_EDGE('',*,*,#16563,.T.);
#23100=ORIENTED_EDGE('',*,*,#16533,.T.);
#23101=ORIENTED_EDGE('',*,*,#16564,.T.);
#23102=ORIENTED_EDGE('',*,*,#16552,.F.);
#23103=ORIENTED_EDGE('',*,*,#16548,.F.);
#23104=ORIENTED_EDGE('',*,*,#16540,.F.);
#23105=ORIENTED_EDGE('',*,*,#16565,.F.);
#23106=ORIENTED_EDGE('',*,*,#16541,.F.);
#23107=ORIENTED_EDGE('',*,*,#16560,.F.);
#23108=ORIENTED_EDGE('',*,*,#16563,.F.);
#23109=ORIENTED_EDGE('',*,*,#16566,.F.);
#23110=ORIENTED_EDGE('',*,*,#16549,.F.);
#23111=ORIENTED_EDGE('',*,*,#16553,.F.);
#23112=ORIENTED_EDGE('',*,*,#16559,.F.);
#23113=ORIENTED_EDGE('',*,*,#16561,.F.);
#23114=ORIENTED_EDGE('',*,*,#16550,.F.);
#23115=ORIENTED_EDGE('',*,*,#16565,.T.);
#23116=ORIENTED_EDGE('',*,*,#16539,.F.);
#23117=ORIENTED_EDGE('',*,*,#16566,.T.);
#23118=ORIENTED_EDGE('',*,*,#16562,.F.);
#23119=ORIENTED_EDGE('',*,*,#16567,.F.);
#23120=ORIENTED_EDGE('',*,*,#16555,.F.);
#23121=ORIENTED_EDGE('',*,*,#16568,.F.);
#23122=ORIENTED_EDGE('',*,*,#16551,.F.);
#23123=ORIENTED_EDGE('',*,*,#16568,.T.);
#23124=ORIENTED_EDGE('',*,*,#16557,.F.);
#23125=ORIENTED_EDGE('',*,*,#16554,.F.);
#23126=ORIENTED_EDGE('',*,*,#16556,.F.);
#23127=ORIENTED_EDGE('',*,*,#16567,.T.);
#23128=ORIENTED_EDGE('',*,*,#16564,.F.);
#23129=ORIENTED_EDGE('',*,*,#16558,.F.);
#26692=ADVANCED_FACE('',(#7868),#1405,.T.);
#26693=ADVANCED_FACE('',(#7869),#1406,.T.);
#26694=ADVANCED_FACE('',(#7870),#1407,.T.);
#26695=ADVANCED_FACE('',(#7871),#1408,.T.);
#26696=ADVANCED_FACE('',(#7872),#1409,.T.);
#26697=ADVANCED_FACE('',(#7873),#381,.F.);
#26698=ADVANCED_FACE('',(#7874),#1410,.T.);
#26699=ADVANCED_FACE('',(#7875),#1411,.T.);
#26700=ADVANCED_FACE('',(#7876),#1412,.T.);
#26701=ADVANCED_FACE('',(#7877),#382,.F.);
#26702=ADVANCED_FACE('',(#7878),#1413,.T.);
#26703=ADVANCED_FACE('',(#7879),#1414,.T.);
#26704=ADVANCED_FACE('',(#7880),#1415,.F.);
#26705=ADVANCED_FACE('',(#7881),#1416,.T.);
#26706=ADVANCED_FACE('',(#7882),#6696,.F.);
#26707=ADVANCED_FACE('',(#7883),#6697,.T.);
#26708=ADVANCED_FACE('',(#7884),#1417,.T.);
#26709=ADVANCED_FACE('',(#7885),#1418,.T.);
#27233=CLOSED_SHELL('',(#26692,#26693,#26694,#26695,#26696,#26697,#26698,
#26699,#26700,#26701,#26702,#26703,#26704,#26705,#26706,#26707,#26708,#26709));
#29223=AXIS2_PLACEMENT_3D('',#45346,#35092,#35093);
#29224=AXIS2_PLACEMENT_3D('',#45347,#35094,#35095);
#29225=AXIS2_PLACEMENT_3D('',#45356,#35098,#35099);
#29226=AXIS2_PLACEMENT_3D('',#45365,#35102,#35103);
#29227=AXIS2_PLACEMENT_3D('',#45368,#35104,#35105);
#29228=AXIS2_PLACEMENT_3D('',#45371,#35108,#35109);
#29229=AXIS2_PLACEMENT_3D('',#45380,#35112,#35113);
#29230=AXIS2_PLACEMENT_3D('',#45389,#35116,#35117);
#29231=AXIS2_PLACEMENT_3D('',#45390,#35118,#35119);
#29232=AXIS2_PLACEMENT_3D('',#45391,#35120,#35121);
#29233=AXIS2_PLACEMENT_3D('',#45392,#35122,#35123);
#29234=AXIS2_PLACEMENT_3D('',#45395,#35124,#35125);
#29235=AXIS2_PLACEMENT_3D('',#45398,#35128,#35129);
#29236=AXIS2_PLACEMENT_3D('',#45401,#35132,#35133);
#29237=AXIS2_PLACEMENT_3D('',#45404,#35134,#35135);
#29238=AXIS2_PLACEMENT_3D('',#45407,#35138,#35139);
#29239=AXIS2_PLACEMENT_3D('',#45408,#35140,#35141);
#29240=AXIS2_PLACEMENT_3D('',#45409,#35142,#35143);
#29241=AXIS2_PLACEMENT_3D('',#45410,#35144,#35145);
#29242=AXIS2_PLACEMENT_3D('',#45413,#35148,#35149);
#29243=AXIS2_PLACEMENT_3D('',#45416,#35150,#35151);
#29244=AXIS2_PLACEMENT_3D('',#45419,#35154,#35155);
#29245=AXIS2_PLACEMENT_3D('',#45420,#35156,#35157);
#29246=AXIS2_PLACEMENT_3D('',#45421,#35158,#35159);
#29247=AXIS2_PLACEMENT_3D('',#45423,#35161,#35162);
#29248=AXIS2_PLACEMENT_3D('',#45424,#35163,#35164);
#29249=AXIS2_PLACEMENT_3D('',#45425,#35165,#35166);
#29250=AXIS2_PLACEMENT_3D('',#45427,#35168,#35169);
#29251=AXIS2_PLACEMENT_3D('',#45428,#35170,#35171);
#35092=DIRECTION('axis',(0.,0.,1.));
#35093=DIRECTION('refdir',(1.,0.,0.));
#35094=DIRECTION('center_axis',(0.553588677216092,-0.6352112172796,-0.53855945437835));
#35095=DIRECTION('ref_axis',(-0.697310151651834,0.,-0.716769525303145));
#35096=DIRECTION('',(0.703080940100181,0.703080940100181,-0.10655694879121));
#35097=DIRECTION('',(0.,-0.646692806155139,0.762750558483697));
#35098=DIRECTION('center_axis',(-0.553588677216093,-0.635211217279596,-0.538559454378353));
#35099=DIRECTION('ref_axis',(-0.697310151651835,0.,0.716769525303144));
#35100=DIRECTION('',(0.,0.646692806155139,-0.762750558483697));
#35101=DIRECTION('',(0.70308094010018,-0.703080940100181,0.10655694879121));
#35102=DIRECTION('center_axis',(-0.707106781186548,-0.707106781186547,0.));
#35103=DIRECTION('ref_axis',(0.,0.,1.));
#35104=DIRECTION('center_axis',(-0.707106781186548,-0.707106781186547,0.));
#35105=DIRECTION('ref_axis',(0.707106781186547,-0.707106781186548,0.));
#35106=DIRECTION('',(0.,0.,-1.));
#35107=DIRECTION('',(0.,0.,1.));
#35108=DIRECTION('center_axis',(0.553588677216087,0.635211217279597,-0.53855945437836));
#35109=DIRECTION('ref_axis',(-0.697310151651843,0.,-0.716769525303136));
#35110=DIRECTION('',(0.,-0.646692806155144,-0.762750558483693));
#35111=DIRECTION('',(-0.703080940100181,0.703080940100181,0.10655694879121));
#35112=DIRECTION('center_axis',(-0.553588677216087,0.635211217279596,-0.53855945437836));
#35113=DIRECTION('ref_axis',(-0.697310151651843,0.,0.716769525303136));
#35114=DIRECTION('',(0.,0.646692806155144,0.762750558483693));
#35115=DIRECTION('',(-0.70308094010018,-0.703080940100181,-0.10655694879121));
#35116=DIRECTION('center_axis',(-1.,0.,0.));
#35117=DIRECTION('ref_axis',(0.,0.159090909090909,-0.987263937680612));
#35118=DIRECTION('center_axis',(-1.,0.,0.));
#35119=DIRECTION('ref_axis',(0.,0.159090909090909,-0.987263937680612));
#35120=DIRECTION('center_axis',(1.,0.,0.));
#35121=DIRECTION('ref_axis',(0.,0.159090909090909,-0.987263937680612));
#35122=DIRECTION('center_axis',(-0.707106781186548,0.707106781186547,0.));
#35123=DIRECTION('ref_axis',(0.,0.,1.));
#35124=DIRECTION('center_axis',(-0.707106781186548,0.707106781186547,0.));
#35125=DIRECTION('ref_axis',(-0.707106781186547,-0.707106781186548,0.));
#35126=DIRECTION('',(0.,0.,-1.));
#35127=DIRECTION('',(0.,0.,1.));
#35128=DIRECTION('center_axis',(0.,0.762750558483693,-0.646692806155144));
#35129=DIRECTION('ref_axis',(-1.,0.,0.));
#35130=DIRECTION('',(-1.,0.,0.));
#35131=DIRECTION('',(1.,0.,0.));
#35132=DIRECTION('center_axis',(0.707106781186548,0.707106781186548,0.));
#35133=DIRECTION('ref_axis',(0.,0.,-1.));
#35134=DIRECTION('center_axis',(0.707106781186548,0.707106781186548,0.));
#35135=DIRECTION('ref_axis',(0.707106781186547,-0.707106781186547,0.));
#35136=DIRECTION('',(0.,0.,-1.));
#35137=DIRECTION('',(0.,0.,1.));
#35138=DIRECTION('center_axis',(1.,0.,0.));
#35139=DIRECTION('ref_axis',(0.,0.159090909090909,-0.987263937680612));
#35140=DIRECTION('center_axis',(1.,0.,0.));
#35141=DIRECTION('ref_axis',(0.,0.159090909090909,-0.987263937680612));
#35142=DIRECTION('center_axis',(-1.,0.,0.));
#35143=DIRECTION('ref_axis',(0.,0.159090909090909,-0.987263937680612));
#35144=DIRECTION('center_axis',(0.,-0.762750558483697,-0.646692806155139));
#35145=DIRECTION('ref_axis',(-1.,0.,0.));
#35146=DIRECTION('',(-1.,0.,0.));
#35147=DIRECTION('',(1.,0.,0.));
#35148=DIRECTION('center_axis',(0.707106781186548,-0.707106781186548,0.));
#35149=DIRECTION('ref_axis',(0.,0.,-1.));
#35150=DIRECTION('center_axis',(0.707106781186548,-0.707106781186548,0.));
#35151=DIRECTION('ref_axis',(-0.707106781186547,-0.707106781186547,0.));
#35152=DIRECTION('',(0.,0.,-1.));
#35153=DIRECTION('',(0.,0.,1.));
#35154=DIRECTION('center_axis',(1.,0.,0.));
#35155=DIRECTION('ref_axis',(0.,0.,-1.));
#35156=DIRECTION('center_axis',(1.,0.,0.));
#35157=DIRECTION('ref_axis',(0.,-0.127272727272727,0.991867759780789));
#35158=DIRECTION('center_axis',(0.,-1.,0.));
#35159=DIRECTION('ref_axis',(0.,0.,-1.));
#35160=DIRECTION('',(1.,0.,0.));
#35161=DIRECTION('center_axis',(1.,0.,0.));
#35162=DIRECTION('ref_axis',(0.,-4.28949804968811E-16,-1.));
#35163=DIRECTION('center_axis',(1.,0.,0.));
#35164=DIRECTION('ref_axis',(0.,1.4130111222502E-16,-1.));
#35165=DIRECTION('center_axis',(1.,0.,0.));
#35166=DIRECTION('ref_axis',(0.,-0.127272727272727,0.991867759780789));
#35167=DIRECTION('',(1.,0.,0.));
#35168=DIRECTION('center_axis',(0.,1.,0.));
#35169=DIRECTION('ref_axis',(0.,0.,1.));
#35170=DIRECTION('center_axis',(1.,0.,0.));
#35171=DIRECTION('ref_axis',(0.,0.,-1.));
#45346=CARTESIAN_POINT('',(0.,0.,0.));
#45347=CARTESIAN_POINT('Origin',(1.8,3.5,21.9198066289735));
#45348=CARTESIAN_POINT('',(1.8,3.5,21.9198066289735));
#45349=CARTESIAN_POINT('',(2.,3.7,21.8894951974686));
#45350=CARTESIAN_POINT('',(1.8,3.5,21.9198066289735));
#45351=CARTESIAN_POINT('',(1.8,3.69730611962488,21.6870912631866));
#45352=CARTESIAN_POINT('',(1.8,3.69730611962488,21.6870912631866));
#45353=CARTESIAN_POINT('Ctrl Pts',(1.79999999999876,3.69730611962487,21.6870912631853));
#45354=CARTESIAN_POINT('Ctrl Pts',(1.89946355488301,3.69863475902964,21.7877634000965));
#45355=CARTESIAN_POINT('Ctrl Pts',(2.,3.7,21.8894951974686));
#45356=CARTESIAN_POINT('Origin',(0.2,3.5,21.9198066289735));
#45357=CARTESIAN_POINT('',(0.2,3.5,21.9198066289735));
#45358=CARTESIAN_POINT('',(0.2,3.69730611962488,21.6870912631866));
#45359=CARTESIAN_POINT('',(0.2,3.5,21.9198066289735));
#45360=CARTESIAN_POINT('',(0.,3.7,21.8894951974686));
#45361=CARTESIAN_POINT('',(0.,3.7,21.8894951974686));
#45362=CARTESIAN_POINT('Ctrl Pts',(-2.94902990916057E-16,3.7,21.8894951974686));
#45363=CARTESIAN_POINT('Ctrl Pts',(0.100536445051347,3.69863475903052,21.7877634001629));
#45364=CARTESIAN_POINT('Ctrl Pts',(0.200000000000001,3.69730611962489,21.6870912631866));
#45365=CARTESIAN_POINT('Origin',(0.1,3.6,13.5822725454788));
#45366=CARTESIAN_POINT('',(0.2,3.5,27.2763633939717));
#45367=CARTESIAN_POINT('',(0.,3.7,27.2499541284018));
#45368=CARTESIAN_POINT('Origin',(3.7,0.,1.21430643318376E-16));
#45369=CARTESIAN_POINT('',(0.,3.7,13.5822725454788));
#45370=CARTESIAN_POINT('',(0.2,3.5,13.5822725454788));
#45371=CARTESIAN_POINT('Origin',(1.8,-3.69730611962489,21.6870912631866));
#45372=CARTESIAN_POINT('',(1.8,-3.69730611962489,21.6870912631866));
#45373=CARTESIAN_POINT('',(2.,-3.7,21.8894951974686));
#45374=CARTESIAN_POINT('Ctrl Pts',(2.,-3.7,21.8894951974686));
#45375=CARTESIAN_POINT('Ctrl Pts',(1.89946355488263,-3.69863475902964,21.7877634000961));
#45376=CARTESIAN_POINT('Ctrl Pts',(1.79999999999876,-3.69730611962488,21.6870912631853));
#45377=CARTESIAN_POINT('',(1.8,-3.5,21.9198066289735));
#45378=CARTESIAN_POINT('',(1.8,-3.5,21.9198066289735));
#45379=CARTESIAN_POINT('',(2.,-3.7,21.8894951974686));
#45380=CARTESIAN_POINT('Origin',(0.2,-3.69730611962489,21.6870912631866));
#45381=CARTESIAN_POINT('',(0.2,-3.69730611962489,21.6870912631866));
#45382=CARTESIAN_POINT('',(0.2,-3.5,21.9198066289735));
#45383=CARTESIAN_POINT('',(0.2,-3.69730611962489,21.6870912631866));
#45384=CARTESIAN_POINT('',(0.,-3.7,21.8894951974686));
#45385=CARTESIAN_POINT('Ctrl Pts',(0.199999999999999,-3.6973061196249,21.6870912631866));
#45386=CARTESIAN_POINT('Ctrl Pts',(0.100536445422227,-3.69863475902553,
21.7877633997876));
#45387=CARTESIAN_POINT('Ctrl Pts',(-9.8879238130678E-16,-3.7,21.8894951974686));
#45388=CARTESIAN_POINT('',(0.2,-3.5,21.9198066289735));
#45389=CARTESIAN_POINT('Origin',(0.1,-2.77555756156289E-16,-8.67361737988404E-16));
#45390=CARTESIAN_POINT('Origin',(0.,-2.77555756156289E-16,-8.67361737988404E-16));
#45391=CARTESIAN_POINT('Origin',(0.2,-2.77555756156289E-16,-8.67361737988404E-16));
#45392=CARTESIAN_POINT('Origin',(0.1,-3.6,10.8039941629797));
#45393=CARTESIAN_POINT('',(0.,-3.7,27.2499541284018));
#45394=CARTESIAN_POINT('',(0.2,-3.5,27.2763633939717));
#45395=CARTESIAN_POINT('Origin',(3.7,0.,1.21430643318376E-16));
#45396=CARTESIAN_POINT('',(0.2,-3.5,10.8039941629797));
#45397=CARTESIAN_POINT('',(0.,-3.7,10.8039941629797));
#45398=CARTESIAN_POINT('Origin',(0.,-3.59865305981244,21.80344894608));
#45399=CARTESIAN_POINT('',(0.,-3.69730611962489,21.6870912631866));
#45400=CARTESIAN_POINT('',(0.,-3.5,21.9198066289735));
#45401=CARTESIAN_POINT('Origin',(1.9,-3.6,10.8039941629797));
#45402=CARTESIAN_POINT('',(1.8,-3.5,27.2763633939717));
#45403=CARTESIAN_POINT('',(2.,-3.7,27.2499541284018));
#45404=CARTESIAN_POINT('Origin',(-1.7,0.,1.21430643318376E-16));
#45405=CARTESIAN_POINT('',(2.,-3.7,10.8039941629797));
#45406=CARTESIAN_POINT('',(1.8,-3.5,10.8039941629797));
#45407=CARTESIAN_POINT('Origin',(1.9,-2.77555756156289E-16,-8.67361737988404E-16));
#45408=CARTESIAN_POINT('Origin',(2.,-2.77555756156289E-16,-8.67361737988404E-16));
#45409=CARTESIAN_POINT('Origin',(1.8,-2.77555756156289E-16,-8.67361737988404E-16));
#45410=CARTESIAN_POINT('Origin',(0.,3.59865305981244,21.80344894608));
#45411=CARTESIAN_POINT('',(0.,3.5,21.9198066289735));
#45412=CARTESIAN_POINT('',(0.,3.69730611962488,21.6870912631866));
#45413=CARTESIAN_POINT('Origin',(1.9,3.6,13.5822725454788));
#45414=CARTESIAN_POINT('',(2.,3.7,27.2499541284018));
#45415=CARTESIAN_POINT('',(1.8,3.5,27.2763633939717));
#45416=CARTESIAN_POINT('Origin',(-1.7,0.,1.21430643318376E-16));
#45417=CARTESIAN_POINT('',(1.8,3.5,13.5822725454788));
#45418=CARTESIAN_POINT('',(2.,3.7,13.5822725454788));
#45419=CARTESIAN_POINT('Origin',(0.,0.,-0.11181830301414));
#45420=CARTESIAN_POINT('Origin',(0.,0.,1.21430643318376E-16));
#45421=CARTESIAN_POINT('Origin',(0.,3.5,27.2763633939717));
#45422=CARTESIAN_POINT('',(0.,3.5,27.2763633939717));
#45423=CARTESIAN_POINT('Origin',(0.,-2.77555756156289E-16,-8.67361737988404E-16));
#45424=CARTESIAN_POINT('Origin',(0.,0.,1.21430643318376E-16));
#45425=CARTESIAN_POINT('Origin',(2.,0.,1.21430643318376E-16));
#45426=CARTESIAN_POINT('',(0.,-3.5,27.2763633939717));
#45427=CARTESIAN_POINT('Origin',(0.,-3.5,21.7198066289735));
#45428=CARTESIAN_POINT('Origin',(2.,0.,-0.11181830301414));
#55707=UNCERTAINTY_MEASURE_WITH_UNIT(LENGTH_MEASURE(0.01),#55738,
'DISTANCE_ACCURACY_VALUE',
'Maximum model space distance between geometric entities at asserted c
onnectivities');
#55715=UNCERTAINTY_MEASURE_WITH_UNIT(LENGTH_MEASURE(0.01),#55738,
'DISTANCE_ACCURACY_VALUE',
'Maximum model space distance between geometric entities at asserted c
onnectivities');
#55729=(
GEOMETRIC_REPRESENTATION_CONTEXT(3)
GLOBAL_UNCERTAINTY_ASSIGNED_CONTEXT((#55707))
GLOBAL_UNIT_ASSIGNED_CONTEXT((#55738,#55740,#55741))
REPRESENTATION_CONTEXT('','3D')
);
#55737=(
GEOMETRIC_REPRESENTATION_CONTEXT(3)
GLOBAL_UNCERTAINTY_ASSIGNED_CONTEXT((#55715))
GLOBAL_UNIT_ASSIGNED_CONTEXT((#55738,#55740,#55741))
REPRESENTATION_CONTEXT('','3D')
);
#55738=(
LENGTH_UNIT()
NAMED_UNIT(*)
SI_UNIT(.MILLI.,.METRE.)
);
#55740=(
NAMED_UNIT(*)
PLANE_ANGLE_UNIT()
SI_UNIT($,.RADIAN.)
);
#55741=(
NAMED_UNIT(*)
SI_UNIT($,.STERADIAN.)
SOLID_ANGLE_UNIT()
);
#55755=SHAPE_DEFINITION_REPRESENTATION(#55776,#55833);
#55776=PRODUCT_DEFINITION_SHAPE('',$,#55855);
#55833=SHAPE_REPRESENTATION('',(#29223),#55729);
#55841=PRODUCT_DEFINITION_CONTEXT('part definition',#55906,'design');
#55855=PRODUCT_DEFINITION('2026-10-26-00-34-27-500',
'13_Circlip_DIN_472_-_52',#55876,#55841);
#55876=PRODUCT_DEFINITION_FORMATION('',$,#55921);
#55906=APPLICATION_CONTEXT(
'Core Data for Automotive Mechanical Design Process');
#55907=PRODUCT_CONTEXT('part definition',#55906,'mechanical');
#55921=PRODUCT('2026-10-26-00-34-27-500','13_Circlip_DIN_472_-_52',$,(#55907));
#55985=COLOUR_RGB('Grey',0.48,0.52,0.57);
#55986=FILL_AREA_STYLE_COLOUR('',#55985);
#55987=FILL_AREA_STYLE('',(#55986));
#55988=SURFACE_STYLE_FILL_AREA(#55987);
#55989=SURFACE_SIDE_STYLE('',(#55988));
#55990=SURFACE_STYLE_USAGE(.BOTH.,#55989);
#55991=PRESENTATION_STYLE_ASSIGNMENT((#55990));
ENDSEC;
END-ISO-10303-21;
